ISO-10303-21;
HEADER;
/* Generated by software containing ST-Developer
 * from STEP Tools, Inc. (www.steptools.com) 
 */

FILE_DESCRIPTION(
/* description */ ('Horizontal push-pull toggle clamp'),
/* implementation_level */ '2;1');

FILE_NAME(
/* name */ 'Hex Bolt - M8x40.step',
/* time_stamp */ '2026-10-27T21:21:09-07:00',
/* author */ (''),
/* organization */ (''),
/* preprocessor_version */ 'ST-DEVELOPER v20.2',
/* originating_system */ 'Autodesk Translation Framework v15.17.0.0',
/* authorisation */ '');

FILE_SCHEMA (('AUTOMOTIVE_DESIGN { 1 0 10303 214 3 1 1 }'));
ENDSEC;

DATA;
#10=MECHANICAL_DESIGN_GEOMETRIC_PRESENTATION_REPRESENTATION('',(#191),#4791);
#18=(
BOUNDED_CURVE()
B_SPLINE_CURVE(2,(#4384,#4385,#4386),.UNSPECIFIED.,.F.,.F.)
B_SPLINE_CURVE_WITH_KNOTS((3,3),(0.14973948338295,0.97160236658079),
 .UNSPECIFIED.)
CURVE()
GEOMETRIC_REPRESENTATION_ITEM()
RATIONAL_B_SPLINE_CURVE((1.07140024848292,1.23714644374248,1.07140024848292))
REPRESENTATION_ITEM('')
);
#19=(
BOUNDED_CURVE()
B_SPLINE_CURVE(2,(#4388,#4389,#4390),.UNSPECIFIED.,.F.,.F.)
B_SPLINE_CURVE_WITH_KNOTS((3,3),(0.14973948338295,0.97160236658079),
 .UNSPECIFIED.)
CURVE()
GEOMETRIC_REPRESENTATION_ITEM()
RATIONAL_B_SPLINE_CURVE((1.07140024848292,1.23714644374248,1.07140024848292))
REPRESENTATION_ITEM('')
);
#20=(
BOUNDED_CURVE()
B_SPLINE_CURVE(2,(#4392,#4393,#4394),.UNSPECIFIED.,.F.,.F.)
B_SPLINE_CURVE_WITH_KNOTS((3,3),(0.14973948338295,0.97160236658079),
 .UNSPECIFIED.)
CURVE()
GEOMETRIC_REPRESENTATION_ITEM()
RATIONAL_B_SPLINE_CURVE((1.07140024848292,1.23714644374248,1.07140024848292))
REPRESENTATION_ITEM('')
);
#21=(
BOUNDED_CURVE()
B_SPLINE_CURVE(2,(#4396,#4397,#4398),.UNSPECIFIED.,.F.,.F.)
B_SPLINE_CURVE_WITH_KNOTS((3,3),(0.149739483382949,0.971602366580789),
 .UNSPECIFIED.)
CURVE()
GEOMETRIC_REPRESENTATION_ITEM()
RATIONAL_B_SPLINE_CURVE((1.07140024848292,1.23714644374248,1.07140024848292))
REPRESENTATION_ITEM('')
);
#22=(
BOUNDED_CURVE()
B_SPLINE_CURVE(2,(#4400,#4401,#4402),.UNSPECIFIED.,.F.,.F.)
B_SPLINE_CURVE_WITH_KNOTS((3,3),(0.14973948338295,0.971602366580789),
 .UNSPECIFIED.)
CURVE()
GEOMETRIC_REPRESENTATION_ITEM()
RATIONAL_B_SPLINE_CURVE((1.07140024848292,1.23714644374248,1.07140024848292))
REPRESENTATION_ITEM('')
);
#23=(
BOUNDED_CURVE()
B_SPLINE_CURVE(2,(#4403,#4404,#4405),.UNSPECIFIED.,.F.,.F.)
B_SPLINE_CURVE_WITH_KNOTS((3,3),(0.14973948338295,0.97160236658079),
 .UNSPECIFIED.)
CURVE()
GEOMETRIC_REPRESENTATION_ITEM()
RATIONAL_B_SPLINE_CURVE((1.07140024848292,1.23714644374248,1.07140024848292))
REPRESENTATION_ITEM('')
);
#151=CONICAL_SURFACE('',#2964,0.36,0.785398163397451);
#152=CONICAL_SURFACE('',#2967,0.734027674973257,1.0471975511966);
#165=SHAPE_REPRESENTATION_RELATIONSHIP('SRR','None',#4871,#178);
#178=ADVANCED_BREP_SHAPE_REPRESENTATION('',(#203),#4784);
#191=STYLED_ITEM('',(#5030),#203);
#203=MANIFOLD_SOLID_BREP('Body1',#2636);
#246=FACE_BOUND('',#665,.T.);
#333=PLANE('',#2966);
#334=PLANE('',#2969);
#335=PLANE('',#2970);
#336=PLANE('',#2971);
#337=PLANE('',#2972);
#338=PLANE('',#2973);
#339=PLANE('',#2974);
#340=PLANE('',#2975);
#341=PLANE('',#2976);
#466=FACE_OUTER_BOUND('',#653,.T.);
#467=FACE_OUTER_BOUND('',#654,.T.);
#468=FACE_OUTER_BOUND('',#655,.T.);
#469=FACE_OUTER_BOUND('',#656,.T.);
#470=FACE_OUTER_BOUND('',#657,.T.);
#471=FACE_OUTER_BOUND('',#658,.T.);
#472=FACE_OUTER_BOUND('',#659,.T.);
#473=FACE_OUTER_BOUND('',#660,.T.);
#474=FACE_OUTER_BOUND('',#661,.T.);
#475=FACE_OUTER_BOUND('',#662,.T.);
#476=FACE_OUTER_BOUND('',#663,.T.);
#477=FACE_OUTER_BOUND('',#664,.T.);
#653=EDGE_LOOP('',(#2257,#2258,#2259,#2260));
#654=EDGE_LOOP('',(#2261,#2262,#2263,#2264));
#655=EDGE_LOOP('',(#2265));
#656=EDGE_LOOP('',(#2266,#2267,#2268,#2269,#2270,#2271,#2272,#2273,#2274));
#657=EDGE_LOOP('',(#2275,#2276,#2277,#2278));
#658=EDGE_LOOP('',(#2279,#2280,#2281,#2282));
#659=EDGE_LOOP('',(#2283,#2284,#2285,#2286));
#660=EDGE_LOOP('',(#2287,#2288,#2289,#2290));
#661=EDGE_LOOP('',(#2291,#2292,#2293,#2294));
#662=EDGE_LOOP('',(#2295,#2296,#2297,#2298));
#663=EDGE_LOOP('',(#2299));
#664=EDGE_LOOP('',(#2300,#2301,#2302,#2303,#2304,#2305));
#665=EDGE_LOOP('',(#2306));
#767=CIRCLE('',#2962,0.3933);
#768=CIRCLE('',#2963,0.3933);
#769=CIRCLE('',#2965,0.32);
#770=CIRCLE('',#2968,0.6175);
#976=LINE('',#4371,#1196);
#977=LINE('',#4376,#1197);
#978=LINE('',#4382,#1198);
#979=LINE('',#4408,#1199);
#980=LINE('',#4410,#1200);
#981=LINE('',#4411,#1201);
#982=LINE('',#4414,#1202);
#983=LINE('',#4415,#1203);
#984=LINE('',#4418,#1204);
#985=LINE('',#4419,#1205);
#986=LINE('',#4422,#1206);
#987=LINE('',#4423,#1207);
#988=LINE('',#4426,#1208);
#989=LINE('',#4427,#1209);
#990=LINE('',#4429,#1210);
#1196=VECTOR('',#3602,0.4);
#1197=VECTOR('',#3609,0.36);
#1198=VECTOR('',#3616,0.734027674973257);
#1199=VECTOR('',#3619,1.);
#1200=VECTOR('',#3620,1.);
#1201=VECTOR('',#3621,1.);
#1202=VECTOR('',#3624,1.);
#1203=VECTOR('',#3625,1.);
#1204=VECTOR('',#3628,1.);
#1205=VECTOR('',#3629,1.);
#1206=VECTOR('',#3632,1.);
#1207=VECTOR('',#3633,1.);
#1208=VECTOR('',#3636,1.);
#1209=VECTOR('',#3637,1.);
#1210=VECTOR('',#3640,1.);
#1393=VERTEX_POINT('',#4368);
#1394=VERTEX_POINT('',#4370);
#1395=VERTEX_POINT('',#4374);
#1396=VERTEX_POINT('',#4379);
#1397=VERTEX_POINT('',#4381);
#1398=VERTEX_POINT('',#4383);
#1399=VERTEX_POINT('',#4387);
#1400=VERTEX_POINT('',#4391);
#1401=VERTEX_POINT('',#4395);
#1402=VERTEX_POINT('',#4399);
#1403=VERTEX_POINT('',#4407);
#1404=VERTEX_POINT('',#4409);
#1405=VERTEX_POINT('',#4413);
#1406=VERTEX_POINT('',#4417);
#1407=VERTEX_POINT('',#4421);
#1408=VERTEX_POINT('',#4425);
#1690=EDGE_CURVE('',#1393,#1393,#767,.F.);
#1691=EDGE_CURVE('',#1393,#1394,#976,.T.);
#1692=EDGE_CURVE('',#1394,#1394,#768,.F.);
#1693=EDGE_CURVE('',#1395,#1395,#769,.T.);
#1694=EDGE_CURVE('',#1395,#1393,#977,.T.);
#1695=EDGE_CURVE('',#1396,#1396,#770,.T.);
#1696=EDGE_CURVE('',#1396,#1397,#978,.T.);
#1697=EDGE_CURVE('',#1398,#1397,#18,.T.);
#1698=EDGE_CURVE('',#1399,#1398,#19,.T.);
#1699=EDGE_CURVE('',#1400,#1399,#20,.T.);
#1700=EDGE_CURVE('',#1401,#1400,#21,.T.);
#1701=EDGE_CURVE('',#1402,#1401,#22,.T.);
#1702=EDGE_CURVE('',#1397,#1402,#23,.T.);
#1703=EDGE_CURVE('',#1403,#1401,#979,.T.);
#1704=EDGE_CURVE('',#1403,#1404,#980,.T.);
#1705=EDGE_CURVE('',#1404,#1402,#981,.T.);
#1706=EDGE_CURVE('',#1405,#1400,#982,.T.);
#1707=EDGE_CURVE('',#1405,#1403,#983,.T.);
#1708=EDGE_CURVE('',#1406,#1399,#984,.T.);
#1709=EDGE_CURVE('',#1406,#1405,#985,.T.);
#1710=EDGE_CURVE('',#1407,#1398,#986,.T.);
#1711=EDGE_CURVE('',#1407,#1406,#987,.T.);
#1712=EDGE_CURVE('',#1408,#1397,#988,.T.);
#1713=EDGE_CURVE('',#1408,#1407,#989,.T.);
#1714=EDGE_CURVE('',#1404,#1408,#990,.T.);
#2257=ORIENTED_EDGE('',*,*,#1690,.F.);
#2258=ORIENTED_EDGE('',*,*,#1691,.T.);
#2259=ORIENTED_EDGE('',*,*,#1692,.F.);
#2260=ORIENTED_EDGE('',*,*,#1691,.F.);
#2261=ORIENTED_EDGE('',*,*,#1693,.F.);
#2262=ORIENTED_EDGE('',*,*,#1694,.T.);
#2263=ORIENTED_EDGE('',*,*,#1690,.T.);
#2264=ORIENTED_EDGE('',*,*,#1694,.F.);
#2265=ORIENTED_EDGE('',*,*,#1693,.T.);
#2266=ORIENTED_EDGE('',*,*,#1695,.F.);
#2267=ORIENTED_EDGE('',*,*,#1696,.T.);
#2268=ORIENTED_EDGE('',*,*,#1697,.F.);
#2269=ORIENTED_EDGE('',*,*,#1698,.F.);
#2270=ORIENTED_EDGE('',*,*,#1699,.F.);
#2271=ORIENTED_EDGE('',*,*,#1700,.F.);
#2272=ORIENTED_EDGE('',*,*,#1701,.F.);
#2273=ORIENTED_EDGE('',*,*,#1702,.F.);
#2274=ORIENTED_EDGE('',*,*,#1696,.F.);
#2275=ORIENTED_EDGE('',*,*,#1701,.T.);
#2276=ORIENTED_EDGE('',*,*,#1703,.F.);
#2277=ORIENTED_EDGE('',*,*,#1704,.T.);
#2278=ORIENTED_EDGE('',*,*,#1705,.T.);
#2279=ORIENTED_EDGE('',*,*,#1700,.T.);
#2280=ORIENTED_EDGE('',*,*,#1706,.F.);
#2281=ORIENTED_EDGE('',*,*,#1707,.T.);
#2282=ORIENTED_EDGE('',*,*,#1703,.T.);
#2283=ORIENTED_EDGE('',*,*,#1699,.T.);
#2284=ORIENTED_EDGE('',*,*,#1708,.F.);
#2285=ORIENTED_EDGE('',*,*,#1709,.T.);
#2286=ORIENTED_EDGE('',*,*,#1706,.T.);
#2287=ORIENTED_EDGE('',*,*,#1698,.T.);
#2288=ORIENTED_EDGE('',*,*,#1710,.F.);
#2289=ORIENTED_EDGE('',*,*,#1711,.T.);
#2290=ORIENTED_EDGE('',*,*,#1708,.T.);
#2291=ORIENTED_EDGE('',*,*,#1697,.T.);
#2292=ORIENTED_EDGE('',*,*,#1712,.F.);
#2293=ORIENTED_EDGE('',*,*,#1713,.T.);
#2294=ORIENTED_EDGE('',*,*,#1710,.T.);
#2295=ORIENTED_EDGE('',*,*,#1702,.T.);
#2296=ORIENTED_EDGE('',*,*,#1705,.F.);
#2297=ORIENTED_EDGE('',*,*,#1714,.T.);
#2298=ORIENTED_EDGE('',*,*,#1712,.T.);
#2299=ORIENTED_EDGE('',*,*,#1695,.T.);
#2300=ORIENTED_EDGE('',*,*,#1709,.F.);
#2301=ORIENTED_EDGE('',*,*,#1711,.F.);
#2302=ORIENTED_EDGE('',*,*,#1713,.F.);
#2303=ORIENTED_EDGE('',*,*,#1714,.F.);
#2304=ORIENTED_EDGE('',*,*,#1704,.F.);
#2305=ORIENTED_EDGE('',*,*,#1707,.F.);
#2306=ORIENTED_EDGE('',*,*,#1692,.T.);
#2467=CYLINDRICAL_SURFACE('',#2961,0.3933);
#2582=ADVANCED_FACE('',(#466),#2467,.T.);
#2583=ADVANCED_FACE('',(#467),#151,.T.);
#2584=ADVANCED_FACE('',(#468),#333,.T.);
#2585=ADVANCED_FACE('',(#469),#152,.T.);
#2586=ADVANCED_FACE('',(#470),#334,.T.);
#2587=ADVANCED_FACE('',(#471),#335,.T.);
#2588=ADVANCED_FACE('',(#472),#336,.T.);
#2589=ADVANCED_FACE('',(#473),#337,.T.);
#2590=ADVANCED_FACE('',(#474),#338,.T.);
#2591=ADVANCED_FACE('',(#475),#339,.T.);
#2592=ADVANCED_FACE('',(#476),#340,.T.);
#2593=ADVANCED_FACE('',(#477,#246),#341,.F.);
#2636=CLOSED_SHELL('',(#2582,#2583,#2584,#2585,#2586,#2587,#2588,#2589,
#2590,#2591,#2592,#2593));
#2960=AXIS2_PLACEMENT_3D('',#4366,#3596,#3597);
#2961=AXIS2_PLACEMENT_3D('',#4367,#3598,#3599);
#2962=AXIS2_PLACEMENT_3D('',#4369,#3600,#3601);
#2963=AXIS2_PLACEMENT_3D('',#4372,#3603,#3604);
#2964=AXIS2_PLACEMENT_3D('',#4373,#3605,#3606);
#2965=AXIS2_PLACEMENT_3D('',#4375,#3607,#3608);
#2966=AXIS2_PLACEMENT_3D('',#4377,#3610,#3611);
#2967=AXIS2_PLACEMENT_3D('',#4378,#3612,#3613);
#2968=AXIS2_PLACEMENT_3D('',#4380,#3614,#3615);
#2969=AXIS2_PLACEMENT_3D('',#4406,#3617,#3618);
#2970=AXIS2_PLACEMENT_3D('',#4412,#3622,#3623);
#2971=AXIS2_PLACEMENT_3D('',#4416,#3626,#3627);
#2972=AXIS2_PLACEMENT_3D('',#4420,#3630,#3631);
#2973=AXIS2_PLACEMENT_3D('',#4424,#3634,#3635);
#2974=AXIS2_PLACEMENT_3D('',#4428,#3638,#3639);
#2975=AXIS2_PLACEMENT_3D('',#4430,#3641,#3642);
#2976=AXIS2_PLACEMENT_3D('',#4431,#3643,#3644);
#3596=DIRECTION('axis',(0.,0.,1.));
#3597=DIRECTION('refdir',(1.,0.,0.));
#3598=DIRECTION('center_axis',(0.,-1.,0.));
#3599=DIRECTION('ref_axis',(1.,0.,0.));
#3600=DIRECTION('center_axis',(0.,1.,0.));
#3601=DIRECTION('ref_axis',(1.,0.,0.));
#3602=DIRECTION('',(0.,1.,0.));
#3603=DIRECTION('center_axis',(0.,-1.,0.));
#3604=DIRECTION('ref_axis',(1.,0.,0.));
#3605=DIRECTION('center_axis',(0.,1.,0.));
#3606=DIRECTION('ref_axis',(1.,0.,0.));
#3607=DIRECTION('center_axis',(0.,-1.,0.));
#3608=DIRECTION('ref_axis',(1.,0.,0.));
#3609=DIRECTION('',(-0.707106781186549,0.707106781186546,-8.65956056235496E-17));
#3610=DIRECTION('center_axis',(0.,-1.,0.));
#3611=DIRECTION('ref_axis',(0.,0.,-1.));
#3612=DIRECTION('center_axis',(0.,-1.,0.));
#3613=DIRECTION('ref_axis',(1.,0.,0.));
#3614=DIRECTION('center_axis',(0.,1.,0.));
#3615=DIRECTION('ref_axis',(1.,0.,0.));
#3616=DIRECTION('',(-0.866025403784439,-0.5,-1.06057523872491E-16));
#3617=DIRECTION('center_axis',(1.4792020664489E-16,0.,-1.));
#3618=DIRECTION('ref_axis',(-1.,0.,-1.4792020664489E-16));
#3619=DIRECTION('',(0.,1.,0.));
#3620=DIRECTION('',(-1.,0.,-1.4792020664489E-16));
#3621=DIRECTION('',(0.,1.,0.));
#3622=DIRECTION('center_axis',(0.866025403784439,0.,-0.5));
#3623=DIRECTION('ref_axis',(-0.5,0.,-0.866025403784439));
#3624=DIRECTION('',(0.,1.,0.));
#3625=DIRECTION('',(-0.5,0.,-0.866025403784439));
#3626=DIRECTION('center_axis',(0.866025403784439,0.,0.5));
#3627=DIRECTION('ref_axis',(0.5,0.,-0.866025403784439));
#3628=DIRECTION('',(0.,1.,0.));
#3629=DIRECTION('',(0.5,0.,-0.866025403784439));
#3630=DIRECTION('center_axis',(-2.95840413289779E-16,0.,1.));
#3631=DIRECTION('ref_axis',(1.,0.,2.95840413289779E-16));
#3632=DIRECTION('',(0.,1.,0.));
#3633=DIRECTION('',(1.,0.,2.95840413289779E-16));
#3634=DIRECTION('center_axis',(-0.866025403784439,0.,0.5));
#3635=DIRECTION('ref_axis',(0.5,0.,0.866025403784439));
#3636=DIRECTION('',(0.,1.,0.));
#3637=DIRECTION('',(0.5,0.,0.866025403784439));
#3638=DIRECTION('center_axis',(-0.866025403784439,0.,-0.5));
#3639=DIRECTION('ref_axis',(-0.5,0.,0.866025403784439));
#3640=DIRECTION('',(-0.5,0.,0.866025403784439));
#3641=DIRECTION('center_axis',(0.,1.,0.));
#3642=DIRECTION('ref_axis',(0.,0.,1.));
#3643=DIRECTION('center_axis',(0.,1.,0.));
#3644=DIRECTION('ref_axis',(1.,0.,0.));
#4366=CARTESIAN_POINT('',(0.,0.,0.));
#4367=CARTESIAN_POINT('Origin',(0.,-1.935,0.));
#4368=CARTESIAN_POINT('',(-0.3933,-3.9267,4.81653586104654E-17));
#4369=CARTESIAN_POINT('Origin',(0.,-3.9267,0.));
#4370=CARTESIAN_POINT('',(-0.3933,0.,-4.81653586104654E-17));
#4371=CARTESIAN_POINT('',(-0.3933,-1.935,-4.81653586104654E-17));
#4372=CARTESIAN_POINT('Origin',(0.,0.,0.));
#4373=CARTESIAN_POINT('Origin',(0.,-3.96,0.));
#4374=CARTESIAN_POINT('',(-0.32,-4.,-3.91886975727153E-17));
#4375=CARTESIAN_POINT('Origin',(0.,-4.,0.));
#4376=CARTESIAN_POINT('',(-0.36,-3.96,-4.40872847693047E-17));
#4377=CARTESIAN_POINT('Origin',(0.,-4.,0.));
#4378=CARTESIAN_POINT('Origin',(0.,0.462722715486149,0.));
#4379=CARTESIAN_POINT('',(-0.6175,0.53,-7.5621939847349E-17));
#4380=CARTESIAN_POINT('Origin',(0.,0.53,0.));
#4381=CARTESIAN_POINT('',(-0.750555349946514,0.453180457891261,-9.19165206894919E-17));
#4382=CARTESIAN_POINT('',(-0.734027674973257,0.462722715486149,-8.98924642641573E-17));
#4383=CARTESIAN_POINT('',(-0.375277674973257,0.453180457891261,0.65));
#4384=CARTESIAN_POINT('Ctrl Pts',(-0.375277674973257,0.45318045789126,0.65));
#4385=CARTESIAN_POINT('Ctrl Pts',(-0.562916512459968,0.561513791224244,
0.324999999999856));
#4386=CARTESIAN_POINT('Ctrl Pts',(-0.750555349946514,0.45318045789126,-9.19165206894919E-17));
#4387=CARTESIAN_POINT('',(0.375277674973257,0.453180457891261,0.65));
#4388=CARTESIAN_POINT('Ctrl Pts',(0.375277674973257,0.453180457891261,0.65));
#4389=CARTESIAN_POINT('Ctrl Pts',(-1.66922031752392E-13,0.561513791224244,
0.65));
#4390=CARTESIAN_POINT('Ctrl Pts',(-0.375277674973257,0.45318045789126,0.65));
#4391=CARTESIAN_POINT('',(0.750555349946514,0.453180457891261,0.));
#4392=CARTESIAN_POINT('Ctrl Pts',(0.750555349946514,0.453180457891261,0.));
#4393=CARTESIAN_POINT('Ctrl Pts',(0.562916512459802,0.561513791224244,0.325000000000144));
#4394=CARTESIAN_POINT('Ctrl Pts',(0.375277674973257,0.45318045789126,0.65));
#4395=CARTESIAN_POINT('',(0.375277674973257,0.453180457891261,-0.65));
#4396=CARTESIAN_POINT('Ctrl Pts',(0.375277674973257,0.45318045789126,-0.65));
#4397=CARTESIAN_POINT('Ctrl Pts',(0.562916512459968,0.561513791224244,-0.324999999999855));
#4398=CARTESIAN_POINT('Ctrl Pts',(0.750555349946514,0.453180457891261,0.));
#4399=CARTESIAN_POINT('',(-0.375277674973257,0.45318045789126,-0.65));
#4400=CARTESIAN_POINT('Ctrl Pts',(-0.375277674973257,0.453180457891261,
-0.65));
#4401=CARTESIAN_POINT('Ctrl Pts',(1.66866520601161E-13,0.561513791224244,
-0.65));
#4402=CARTESIAN_POINT('Ctrl Pts',(0.375277674973257,0.45318045789126,-0.65));
#4403=CARTESIAN_POINT('Ctrl Pts',(-0.750555349946514,0.453180457891261,
-9.19165206894919E-17));
#4404=CARTESIAN_POINT('Ctrl Pts',(-0.562916512459802,0.561513791224244,
-0.325000000000144));
#4405=CARTESIAN_POINT('Ctrl Pts',(-0.375277674973257,0.45318045789126,-0.65));
#4406=CARTESIAN_POINT('Origin',(0.375277674973257,0.,-0.65));
#4407=CARTESIAN_POINT('',(0.375277674973257,0.,-0.65));
#4408=CARTESIAN_POINT('',(0.375277674973257,0.,-0.65));
#4409=CARTESIAN_POINT('',(-0.375277674973257,0.,-0.65));
#4410=CARTESIAN_POINT('',(0.375277674973257,0.,-0.65));
#4411=CARTESIAN_POINT('',(-0.375277674973257,0.,-0.65));
#4412=CARTESIAN_POINT('Origin',(0.750555349946514,0.,0.));
#4413=CARTESIAN_POINT('',(0.750555349946514,0.,0.));
#4414=CARTESIAN_POINT('',(0.750555349946514,0.,0.));
#4415=CARTESIAN_POINT('',(0.750555349946514,0.,0.));
#4416=CARTESIAN_POINT('Origin',(0.375277674973257,0.,0.65));
#4417=CARTESIAN_POINT('',(0.375277674973257,0.,0.65));
#4418=CARTESIAN_POINT('',(0.375277674973257,0.,0.65));
#4419=CARTESIAN_POINT('',(0.375277674973257,0.,0.65));
#4420=CARTESIAN_POINT('Origin',(-0.375277674973257,0.,0.65));
#4421=CARTESIAN_POINT('',(-0.375277674973257,0.,0.65));
#4422=CARTESIAN_POINT('',(-0.375277674973257,0.,0.65));
#4423=CARTESIAN_POINT('',(-0.375277674973257,0.,0.65));
#4424=CARTESIAN_POINT('Origin',(-0.750555349946514,0.,-9.19165206894919E-17));
#4425=CARTESIAN_POINT('',(-0.750555349946514,0.,-9.19165206894919E-17));
#4426=CARTESIAN_POINT('',(-0.750555349946514,0.,-9.19165206894919E-17));
#4427=CARTESIAN_POINT('',(-0.750555349946514,0.,-9.19165206894919E-17));
#4428=CARTESIAN_POINT('Origin',(-0.375277674973257,0.,-0.65));
#4429=CARTESIAN_POINT('',(-0.375277674973257,0.,-0.65));
#4430=CARTESIAN_POINT('Origin',(0.,0.53,-1.11022302462516E-16));
#4431=CARTESIAN_POINT('Origin',(0.,0.,-1.11022302462516E-16));
#4765=UNCERTAINTY_MEASURE_WITH_UNIT(LENGTH_MEASURE(0.001),#4792,
'DISTANCE_ACCURACY_VALUE',
'Maximum model space distance between geometric entities at asserted c
onnectivities');
#4772=UNCERTAINTY_MEASURE_WITH_UNIT(LENGTH_MEASURE(0.001),#4792,
'DISTANCE_ACCURACY_VALUE',
'Maximum model space distance between geometric entities at asserted c
onnectivities');
#4784=(
GEOMETRIC_REPRESENTATION_CONTEXT(3)
GLOBAL_UNCERTAINTY_ASSIGNED_CONTEXT((#4765))
GLOBAL_UNIT_ASSIGNED_CONTEXT((#4792,#4794,#4795))
REPRESENTATION_CONTEXT('','3D')
);
#4791=(
GEOMETRIC_REPRESENTATION_CONTEXT(3)
GLOBAL_UNCERTAINTY_ASSIGNED_CONTEXT((#4772))
GLOBAL_UNIT_ASSIGNED_CONTEXT((#4792,#4794,#4795))
REPRESENTATION_CONTEXT('','3D')
);
#4792=(
LENGTH_UNIT()
NAMED_UNIT(*)
SI_UNIT(.CENTI.,.METRE.)
);
#4794=(
NAMED_UNIT(*)
PLANE_ANGLE_UNIT()
SI_UNIT($,.RADIAN.)
);
#4795=(
NAMED_UNIT(*)
SI_UNIT($,.STERADIAN.)
SOLID_ANGLE_UNIT()
);
#4807=SHAPE_DEFINITION_REPRESENTATION(#4826,#4871);
#4826=PRODUCT_DEFINITION_SHAPE('',$,#4890);
#4871=SHAPE_REPRESENTATION('',(#2960),#4784);
#4878=PRODUCT_DEFINITION_CONTEXT('part definition',#4934,'design');
#4890=PRODUCT_DEFINITION('Hex Bolt - M8x40','Hex Bolt - M8x40',#4908,#4878);
#4908=PRODUCT_DEFINITION_FORMATION('',$,#4947);
#4934=APPLICATION_CONTEXT(
'Core Data for Automotive Mechanical Design Process');
#4935=PRODUCT_CONTEXT('part definition',#4934,'mechanical');
#4947=PRODUCT('Hex Bolt - M8x40','Hex Bolt - M8x40','Hex Bolt - M8x40',
(#4935));
#5024=COLOUR_RGB('Black',0.12,0.14,0.17);
#5025=FILL_AREA_STYLE_COLOUR('',#5024);
#5026=FILL_AREA_STYLE('',(#5025));
#5027=SURFACE_STYLE_FILL_AREA(#5026);
#5028=SURFACE_SIDE_STYLE('',(#5027));
#5029=SURFACE_STYLE_USAGE(.BOTH.,#5028);
#5030=PRESENTATION_STYLE_ASSIGNMENT((#5029));
ENDSEC;
END-ISO-10303-21;
